ISO-10303-21;
HEADER;
/* Generated by software containing ST-Developer
 * from STEP Tools, Inc. (www.steptools.com) 
 */

FILE_DESCRIPTION(
/* description */ (''),
/* implementation_level */ '2;1');

FILE_NAME(
/* name */ 'Binding Head Screw JIS B 1111 - M2x6 Steel 4.6 Plain v1 (2).step',
/* time_stamp */ '2026-10-07T02:13:48+06:00',
/* author */ (''),
/* organization */ (''),
/* preprocessor_version */ 'ST-DEVELOPER v20.2',
/* originating_system */ 'Autodesk Translation Framework v15.15.0.0',
/* authorisation */ '');

FILE_SCHEMA (('AUTOMOTIVE_DESIGN { 1 0 10303 214 3 1 1 }'));
ENDSEC;

DATA;
#10=MECHANICAL_DESIGN_GEOMETRIC_PRESENTATION_REPRESENTATION('',(#123),#17042);
#64=CONICAL_SURFACE('',#9107,0.919615242270664,0.261799387799148);
#65=CONICAL_SURFACE('',#9116,2.11281731799709,0.0872664626099693);
#99=SHAPE_REPRESENTATION_RELATIONSHIP('SRR','None',#17095,#111);
#111=ADVANCED_BREP_SHAPE_REPRESENTATION('',(#135),#17039);
#123=STYLED_ITEM('',(#17154),#135);
#135=MANIFOLD_SOLID_BREP('Body1',#8124);
#175=FACE_BOUND('',#1411,.T.);
#211=SPHERICAL_SURFACE('',#9112,6.32965591734106);
#234=TOROIDAL_SURFACE('',#9099,0.939230484541328,0.1);
#260=ELLIPSE('',#9058,0.992,0.496);
#261=ELLIPSE('',#9060,0.992,0.496);
#262=ELLIPSE('',#9065,0.992,0.496);
#263=ELLIPSE('',#9070,0.992,0.496);
#264=ELLIPSE('',#9075,0.992,0.496);
#265=ELLIPSE('',#9079,0.992,0.496);
#266=ELLIPSE('',#9081,0.992,0.496);
#267=ELLIPSE('',#9086,0.992,0.496);
#431=PLANE('',#9061);
#432=PLANE('',#9063);
#433=PLANE('',#9066);
#434=PLANE('',#9071);
#435=PLANE('',#9073);
#436=PLANE('',#9076);
#437=PLANE('',#9082);
#438=PLANE('',#9087);
#439=PLANE('',#9089);
#440=PLANE('',#9091);
#441=PLANE('',#9094);
#442=PLANE('',#9096);
#443=PLANE('',#9098);
#444=PLANE('',#9103);
#445=PLANE('',#9111);
#878=FACE_OUTER_BOUND('',#1392,.T.);
#879=FACE_OUTER_BOUND('',#1393,.T.);
#880=FACE_OUTER_BOUND('',#1394,.T.);
#881=FACE_OUTER_BOUND('',#1395,.T.);
#882=FACE_OUTER_BOUND('',#1396,.T.);
#883=FACE_OUTER_BOUND('',#1397,.T.);
#884=FACE_OUTER_BOUND('',#1398,.T.);
#885=FACE_OUTER_BOUND('',#1399,.T.);
#886=FACE_OUTER_BOUND('',#1400,.T.);
#887=FACE_OUTER_BOUND('',#1401,.T.);
#888=FACE_OUTER_BOUND('',#1402,.T.);
#889=FACE_OUTER_BOUND('',#1403,.T.);
#890=FACE_OUTER_BOUND('',#1404,.T.);
#891=FACE_OUTER_BOUND('',#1405,.T.);
#892=FACE_OUTER_BOUND('',#1406,.T.);
#893=FACE_OUTER_BOUND('',#1407,.T.);
#894=FACE_OUTER_BOUND('',#1408,.T.);
#895=FACE_OUTER_BOUND('',#1409,.T.);
#896=FACE_OUTER_BOUND('',#1410,.T.);
#897=FACE_OUTER_BOUND('',#1412,.T.);
#898=FACE_OUTER_BOUND('',#1413,.T.);
#899=FACE_OUTER_BOUND('',#1414,.T.);
#900=FACE_OUTER_BOUND('',#1415,.T.);
#901=FACE_OUTER_BOUND('',#1416,.T.);
#902=FACE_OUTER_BOUND('',#1417,.T.);
#1392=EDGE_LOOP('',(#7065,#7066,#7067,#7068,#7069,#7070));
#1393=EDGE_LOOP('',(#7071,#7072,#7073));
#1394=EDGE_LOOP('',(#7074,#7075,#7076,#7077,#7078,#7079));
#1395=EDGE_LOOP('',(#7080,#7081,#7082));
#1396=EDGE_LOOP('',(#7083,#7084,#7085,#7086,#7087,#7088));
#1397=EDGE_LOOP('',(#7089,#7090,#7091));
#1398=EDGE_LOOP('',(#7092,#7093,#7094,#7095,#7096,#7097));
#1399=EDGE_LOOP('',(#7098,#7099,#7100));
#1400=EDGE_LOOP('',(#7101,#7102,#7103,#7104,#7105,#7106));
#1401=EDGE_LOOP('',(#7107,#7108,#7109));
#1402=EDGE_LOOP('',(#7110,#7111,#7112,#7113,#7114,#7115));
#1403=EDGE_LOOP('',(#7116,#7117,#7118));
#1404=EDGE_LOOP('',(#7119,#7120,#7121));
#1405=EDGE_LOOP('',(#7122,#7123,#7124,#7125,#7126,#7127,#7128));
#1406=EDGE_LOOP('',(#7129,#7130,#7131));
#1407=EDGE_LOOP('',(#7132,#7133,#7134,#7135,#7136,#7137));
#1408=EDGE_LOOP('',(#7138,#7139,#7140,#7141,#7142,#7143,#7144,#7145));
#1409=EDGE_LOOP('',(#7146,#7147,#7148,#7149));
#1410=EDGE_LOOP('',(#7150));
#1411=EDGE_LOOP('',(#7151));
#1412=EDGE_LOOP('',(#7152,#7153,#7154,#7155));
#1413=EDGE_LOOP('',(#7156,#7157,#7158,#7159));
#1414=EDGE_LOOP('',(#7160,#7161,#7162,#7163));
#1415=EDGE_LOOP('',(#7164));
#1416=EDGE_LOOP('',(#7165,#7166,#7167,#7168,#7169,#7170,#7171,#7172,#7173,
#7174,#7175,#7176,#7177,#7178,#7179,#7180,#7181,#7182,#7183,#7184,#7185));
#1417=EDGE_LOOP('',(#7186,#7187,#7188,#7189,#7190));
#1869=CIRCLE('',#9059,0.496);
#1870=CIRCLE('',#9062,6.32479565138939);
#1871=CIRCLE('',#9064,5.93049029404341);
#1872=CIRCLE('',#9067,6.32479565138933);
#1873=CIRCLE('',#9069,0.496);
#1874=CIRCLE('',#9072,6.32479565138941);
#1875=CIRCLE('',#9074,5.93049029404341);
#1876=CIRCLE('',#9077,6.32479565138941);
#1877=CIRCLE('',#9080,0.496);
#1878=CIRCLE('',#9083,6.32479565138943);
#1879=CIRCLE('',#9085,0.496);
#1880=CIRCLE('',#9088,6.32479565138944);
#1881=CIRCLE('',#9090,6.32479565138933);
#1882=CIRCLE('',#9092,5.93049029404347);
#1883=CIRCLE('',#9093,5.93049029404347);
#1884=CIRCLE('',#9095,6.32479565138944);
#1885=CIRCLE('',#9097,5.93049029404341);
#1886=CIRCLE('',#9100,0.939230484541328);
#1887=CIRCLE('',#9101,0.1);
#1888=CIRCLE('',#9102,0.839230484541328);
#1889=CIRCLE('',#9104,2.15);
#1890=CIRCLE('',#9106,0.839230484541328);
#1891=CIRCLE('',#9108,0.96675);
#1892=CIRCLE('',#9110,0.96675);
#1893=CIRCLE('',#9113,6.32965591734106);
#1894=CIRCLE('',#9114,2.07563463599418);
#1895=CIRCLE('',#9115,2.07563463599418);
#2010=B_SPLINE_CURVE_WITH_KNOTS('',3,(#16449,#16450,#16451,#16452,#16453,
#16454,#16455,#16456,#16457,#16458,#16459,#16460,#16461,#16462,#16463),
 .UNSPECIFIED.,.F.,.F.,(4,2,2,3,2,2,4),(-0.0374758352523592,-0.0373394553501654,
-0.0186697276750827,0.,0.0186697276750831,0.0373394553501661,0.0374758352523223),
 .UNSPECIFIED.);
#2011=B_SPLINE_CURVE_WITH_KNOTS('',3,(#16491,#16492,#16493,#16494,#16495,
#16496,#16497,#16498,#16499,#16500,#16501,#16502,#16503,#16504,#16505),
 .UNSPECIFIED.,.F.,.F.,(4,2,2,3,2,2,4),(-0.0374758352523656,-0.0373394553501654,
-0.0186697276750827,0.,0.0186697276750831,0.0373394553501662,0.0374758352523289),
 .UNSPECIFIED.);
#2012=B_SPLINE_CURVE_WITH_KNOTS('',3,(#16530,#16531,#16532,#16533,#16534,
#16535,#16536,#16537,#16538,#16539,#16540,#16541,#16542,#16543,#16544),
 .UNSPECIFIED.,.F.,.F.,(4,2,2,3,2,2,4),(-0.0374758352524519,-0.0373394553501659,
-0.0186697276750829,0.,0.0186697276750829,0.0373394553501658,0.0374758352524142),
 .UNSPECIFIED.);
#2013=B_SPLINE_CURVE_WITH_KNOTS('',3,(#16560,#16561,#16562,#16563,#16564,
#16565,#16566,#16567,#16568,#16569,#16570,#16571,#16572,#16573,#16574),
 .UNSPECIFIED.,.F.,.F.,(4,2,2,3,2,2,4),(-0.0374758352524171,-0.0373394553501658,
-0.0186697276750829,0.,0.018669727675083,0.037339455350166,0.0374758352523797),
 .UNSPECIFIED.);
#2528=LINE('',#16465,#3106);
#2529=LINE('',#16472,#3107);
#2530=LINE('',#16476,#3108);
#2531=LINE('',#16481,#3109);
#2532=LINE('',#16484,#3110);
#2533=LINE('',#16488,#3111);
#2534=LINE('',#16510,#3112);
#2535=LINE('',#16514,#3113);
#2536=LINE('',#16519,#3114);
#2537=LINE('',#16522,#3115);
#2538=LINE('',#16526,#3116);
#2539=LINE('',#16546,#3117);
#2540=LINE('',#16553,#3118);
#2541=LINE('',#16557,#3119);
#2542=LINE('',#16579,#3120);
#2543=LINE('',#16583,#3121);
#2544=LINE('',#16587,#3122);
#2545=LINE('',#16591,#3123);
#2546=LINE('',#16596,#3124);
#2547=LINE('',#16599,#3125);
#2548=LINE('',#16613,#3126);
#2549=LINE('',#16617,#3127);
#2550=LINE('',#16621,#3128);
#2551=LINE('',#16630,#3129);
#3106=VECTOR('',#11353,10.);
#3107=VECTOR('',#11360,10.);
#3108=VECTOR('',#11365,10.);
#3109=VECTOR('',#11370,10.);
#3110=VECTOR('',#11373,10.);
#3111=VECTOR('',#11378,10.);
#3112=VECTOR('',#11385,10.);
#3113=VECTOR('',#11390,10.);
#3114=VECTOR('',#11395,10.);
#3115=VECTOR('',#11398,10.);
#3116=VECTOR('',#11403,10.);
#3117=VECTOR('',#11406,10.);
#3118=VECTOR('',#11413,10.);
#3119=VECTOR('',#11418,10.);
#3120=VECTOR('',#11425,10.);
#3121=VECTOR('',#11430,10.);
#3122=VECTOR('',#11435,10.);
#3123=VECTOR('',#11440,10.);
#3124=VECTOR('',#11447,10.);
#3125=VECTOR('',#11452,10.);
#3126=VECTOR('',#11471,0.839230484541328);
#3127=VECTOR('',#11476,0.919615242270664);
#3128=VECTOR('',#11481,1.);
#3129=VECTOR('',#11494,2.11281731799709);
#3789=VERTEX_POINT('',#16447);
#3790=VERTEX_POINT('',#16448);
#3791=VERTEX_POINT('',#16464);
#3792=VERTEX_POINT('',#16466);
#3793=VERTEX_POINT('',#16468);
#3794=VERTEX_POINT('',#16470);
#3795=VERTEX_POINT('',#16474);
#3796=VERTEX_POINT('',#16478);
#3797=VERTEX_POINT('',#16480);
#3798=VERTEX_POINT('',#16482);
#3799=VERTEX_POINT('',#16486);
#3800=VERTEX_POINT('',#16490);
#3801=VERTEX_POINT('',#16506);
#3802=VERTEX_POINT('',#16508);
#3803=VERTEX_POINT('',#16512);
#3804=VERTEX_POINT('',#16516);
#3805=VERTEX_POINT('',#16518);
#3806=VERTEX_POINT('',#16520);
#3807=VERTEX_POINT('',#16524);
#3808=VERTEX_POINT('',#16528);
#3809=VERTEX_POINT('',#16529);
#3810=VERTEX_POINT('',#16545);
#3811=VERTEX_POINT('',#16547);
#3812=VERTEX_POINT('',#16549);
#3813=VERTEX_POINT('',#16551);
#3814=VERTEX_POINT('',#16555);
#3815=VERTEX_POINT('',#16559);
#3816=VERTEX_POINT('',#16575);
#3817=VERTEX_POINT('',#16577);
#3818=VERTEX_POINT('',#16581);
#3819=VERTEX_POINT('',#16585);
#3820=VERTEX_POINT('',#16589);
#3821=VERTEX_POINT('',#16594);
#3822=VERTEX_POINT('',#16602);
#3823=VERTEX_POINT('',#16604);
#3824=VERTEX_POINT('',#16608);
#3825=VERTEX_POINT('',#16611);
#3826=VERTEX_POINT('',#16615);
#3827=VERTEX_POINT('',#16619);
#3828=VERTEX_POINT('',#16624);
#3829=VERTEX_POINT('',#16626);
#4900=EDGE_CURVE('',#3789,#3790,#2010,.T.);
#4901=EDGE_CURVE('',#3791,#3789,#2528,.T.);
#4902=EDGE_CURVE('',#3791,#3792,#260,.F.);
#4903=EDGE_CURVE('',#3792,#3793,#1869,.F.);
#4904=EDGE_CURVE('',#3794,#3793,#261,.T.);
#4905=EDGE_CURVE('',#3790,#3794,#2529,.T.);
#4906=EDGE_CURVE('',#3790,#3795,#1870,.T.);
#4907=EDGE_CURVE('',#3795,#3794,#2530,.F.);
#4908=EDGE_CURVE('',#3795,#3796,#1871,.T.);
#4909=EDGE_CURVE('',#3793,#3797,#2531,.F.);
#4910=EDGE_CURVE('',#3798,#3797,#262,.F.);
#4911=EDGE_CURVE('',#3796,#3798,#2532,.T.);
#4912=EDGE_CURVE('',#3796,#3799,#1872,.T.);
#4913=EDGE_CURVE('',#3798,#3799,#2533,.T.);
#4914=EDGE_CURVE('',#3799,#3800,#2011,.T.);
#4915=EDGE_CURVE('',#3797,#3801,#1873,.F.);
#4916=EDGE_CURVE('',#3802,#3801,#263,.T.);
#4917=EDGE_CURVE('',#3800,#3802,#2534,.T.);
#4918=EDGE_CURVE('',#3800,#3803,#1874,.T.);
#4919=EDGE_CURVE('',#3803,#3802,#2535,.F.);
#4920=EDGE_CURVE('',#3803,#3804,#1875,.T.);
#4921=EDGE_CURVE('',#3801,#3805,#2536,.F.);
#4922=EDGE_CURVE('',#3806,#3805,#264,.F.);
#4923=EDGE_CURVE('',#3804,#3806,#2537,.T.);
#4924=EDGE_CURVE('',#3804,#3807,#1876,.T.);
#4925=EDGE_CURVE('',#3806,#3807,#2538,.T.);
#4926=EDGE_CURVE('',#3808,#3809,#2012,.T.);
#4927=EDGE_CURVE('',#3810,#3808,#2539,.T.);
#4928=EDGE_CURVE('',#3810,#3811,#265,.F.);
#4929=EDGE_CURVE('',#3811,#3812,#1877,.F.);
#4930=EDGE_CURVE('',#3813,#3812,#266,.T.);
#4931=EDGE_CURVE('',#3809,#3813,#2540,.T.);
#4932=EDGE_CURVE('',#3809,#3814,#1878,.T.);
#4933=EDGE_CURVE('',#3814,#3813,#2541,.F.);
#4934=EDGE_CURVE('',#3807,#3815,#2013,.T.);
#4935=EDGE_CURVE('',#3805,#3816,#1879,.F.);
#4936=EDGE_CURVE('',#3817,#3816,#267,.T.);
#4937=EDGE_CURVE('',#3815,#3817,#2542,.T.);
#4938=EDGE_CURVE('',#3815,#3818,#1880,.T.);
#4939=EDGE_CURVE('',#3818,#3817,#2543,.F.);
#4940=EDGE_CURVE('',#3819,#3789,#1881,.T.);
#4941=EDGE_CURVE('',#3819,#3791,#2544,.T.);
#4942=EDGE_CURVE('',#3814,#3820,#1882,.T.);
#4943=EDGE_CURVE('',#3812,#3792,#2545,.F.);
#4944=EDGE_CURVE('',#3820,#3819,#1883,.T.);
#4945=EDGE_CURVE('',#3821,#3808,#1884,.T.);
#4946=EDGE_CURVE('',#3821,#3810,#2546,.T.);
#4947=EDGE_CURVE('',#3818,#3821,#1885,.T.);
#4948=EDGE_CURVE('',#3816,#3811,#2547,.F.);
#4949=EDGE_CURVE('',#3822,#3822,#1886,.T.);
#4950=EDGE_CURVE('',#3822,#3823,#1887,.T.);
#4951=EDGE_CURVE('',#3823,#3823,#1888,.T.);
#4952=EDGE_CURVE('',#3824,#3824,#1889,.T.);
#4953=EDGE_CURVE('',#3825,#3825,#1890,.T.);
#4954=EDGE_CURVE('',#3825,#3823,#2548,.T.);
#4955=EDGE_CURVE('',#3826,#3826,#1891,.T.);
#4956=EDGE_CURVE('',#3826,#3825,#2549,.T.);
#4957=EDGE_CURVE('',#3827,#3827,#1892,.F.);
#4958=EDGE_CURVE('',#3827,#3826,#2550,.T.);
#4959=EDGE_CURVE('',#3820,#3828,#1893,.T.);
#4960=EDGE_CURVE('',#3829,#3828,#1894,.T.);
#4961=EDGE_CURVE('',#3828,#3829,#1895,.T.);
#4962=EDGE_CURVE('',#3824,#3829,#2551,.T.);
#7065=ORIENTED_EDGE('',*,*,#4900,.F.);
#7066=ORIENTED_EDGE('',*,*,#4901,.F.);
#7067=ORIENTED_EDGE('',*,*,#4902,.T.);
#7068=ORIENTED_EDGE('',*,*,#4903,.T.);
#7069=ORIENTED_EDGE('',*,*,#4904,.F.);
#7070=ORIENTED_EDGE('',*,*,#4905,.F.);
#7071=ORIENTED_EDGE('',*,*,#4906,.F.);
#7072=ORIENTED_EDGE('',*,*,#4905,.T.);
#7073=ORIENTED_EDGE('',*,*,#4907,.F.);
#7074=ORIENTED_EDGE('',*,*,#4908,.F.);
#7075=ORIENTED_EDGE('',*,*,#4907,.T.);
#7076=ORIENTED_EDGE('',*,*,#4904,.T.);
#7077=ORIENTED_EDGE('',*,*,#4909,.T.);
#7078=ORIENTED_EDGE('',*,*,#4910,.F.);
#7079=ORIENTED_EDGE('',*,*,#4911,.F.);
#7080=ORIENTED_EDGE('',*,*,#4912,.F.);
#7081=ORIENTED_EDGE('',*,*,#4911,.T.);
#7082=ORIENTED_EDGE('',*,*,#4913,.T.);
#7083=ORIENTED_EDGE('',*,*,#4914,.F.);
#7084=ORIENTED_EDGE('',*,*,#4913,.F.);
#7085=ORIENTED_EDGE('',*,*,#4910,.T.);
#7086=ORIENTED_EDGE('',*,*,#4915,.T.);
#7087=ORIENTED_EDGE('',*,*,#4916,.F.);
#7088=ORIENTED_EDGE('',*,*,#4917,.F.);
#7089=ORIENTED_EDGE('',*,*,#4918,.F.);
#7090=ORIENTED_EDGE('',*,*,#4917,.T.);
#7091=ORIENTED_EDGE('',*,*,#4919,.F.);
#7092=ORIENTED_EDGE('',*,*,#4920,.F.);
#7093=ORIENTED_EDGE('',*,*,#4919,.T.);
#7094=ORIENTED_EDGE('',*,*,#4916,.T.);
#7095=ORIENTED_EDGE('',*,*,#4921,.T.);
#7096=ORIENTED_EDGE('',*,*,#4922,.F.);
#7097=ORIENTED_EDGE('',*,*,#4923,.F.);
#7098=ORIENTED_EDGE('',*,*,#4924,.F.);
#7099=ORIENTED_EDGE('',*,*,#4923,.T.);
#7100=ORIENTED_EDGE('',*,*,#4925,.T.);
#7101=ORIENTED_EDGE('',*,*,#4926,.F.);
#7102=ORIENTED_EDGE('',*,*,#4927,.F.);
#7103=ORIENTED_EDGE('',*,*,#4928,.T.);
#7104=ORIENTED_EDGE('',*,*,#4929,.T.);
#7105=ORIENTED_EDGE('',*,*,#4930,.F.);
#7106=ORIENTED_EDGE('',*,*,#4931,.F.);
#7107=ORIENTED_EDGE('',*,*,#4932,.F.);
#7108=ORIENTED_EDGE('',*,*,#4931,.T.);
#7109=ORIENTED_EDGE('',*,*,#4933,.F.);
#7110=ORIENTED_EDGE('',*,*,#4934,.F.);
#7111=ORIENTED_EDGE('',*,*,#4925,.F.);
#7112=ORIENTED_EDGE('',*,*,#4922,.T.);
#7113=ORIENTED_EDGE('',*,*,#4935,.T.);
#7114=ORIENTED_EDGE('',*,*,#4936,.F.);
#7115=ORIENTED_EDGE('',*,*,#4937,.F.);
#7116=ORIENTED_EDGE('',*,*,#4938,.F.);
#7117=ORIENTED_EDGE('',*,*,#4937,.T.);
#7118=ORIENTED_EDGE('',*,*,#4939,.F.);
#7119=ORIENTED_EDGE('',*,*,#4940,.F.);
#7120=ORIENTED_EDGE('',*,*,#4941,.T.);
#7121=ORIENTED_EDGE('',*,*,#4901,.T.);
#7122=ORIENTED_EDGE('',*,*,#4942,.F.);
#7123=ORIENTED_EDGE('',*,*,#4933,.T.);
#7124=ORIENTED_EDGE('',*,*,#4930,.T.);
#7125=ORIENTED_EDGE('',*,*,#4943,.T.);
#7126=ORIENTED_EDGE('',*,*,#4902,.F.);
#7127=ORIENTED_EDGE('',*,*,#4941,.F.);
#7128=ORIENTED_EDGE('',*,*,#4944,.F.);
#7129=ORIENTED_EDGE('',*,*,#4945,.F.);
#7130=ORIENTED_EDGE('',*,*,#4946,.T.);
#7131=ORIENTED_EDGE('',*,*,#4927,.T.);
#7132=ORIENTED_EDGE('',*,*,#4947,.F.);
#7133=ORIENTED_EDGE('',*,*,#4939,.T.);
#7134=ORIENTED_EDGE('',*,*,#4936,.T.);
#7135=ORIENTED_EDGE('',*,*,#4948,.T.);
#7136=ORIENTED_EDGE('',*,*,#4928,.F.);
#7137=ORIENTED_EDGE('',*,*,#4946,.F.);
#7138=ORIENTED_EDGE('',*,*,#4909,.F.);
#7139=ORIENTED_EDGE('',*,*,#4903,.F.);
#7140=ORIENTED_EDGE('',*,*,#4943,.F.);
#7141=ORIENTED_EDGE('',*,*,#4929,.F.);
#7142=ORIENTED_EDGE('',*,*,#4948,.F.);
#7143=ORIENTED_EDGE('',*,*,#4935,.F.);
#7144=ORIENTED_EDGE('',*,*,#4921,.F.);
#7145=ORIENTED_EDGE('',*,*,#4915,.F.);
#7146=ORIENTED_EDGE('',*,*,#4949,.T.);
#7147=ORIENTED_EDGE('',*,*,#4950,.T.);
#7148=ORIENTED_EDGE('',*,*,#4951,.T.);
#7149=ORIENTED_EDGE('',*,*,#4950,.F.);
#7150=ORIENTED_EDGE('',*,*,#4952,.T.);
#7151=ORIENTED_EDGE('',*,*,#4949,.F.);
#7152=ORIENTED_EDGE('',*,*,#4953,.F.);
#7153=ORIENTED_EDGE('',*,*,#4954,.T.);
#7154=ORIENTED_EDGE('',*,*,#4951,.F.);
#7155=ORIENTED_EDGE('',*,*,#4954,.F.);
#7156=ORIENTED_EDGE('',*,*,#4955,.F.);
#7157=ORIENTED_EDGE('',*,*,#4956,.T.);
#7158=ORIENTED_EDGE('',*,*,#4953,.T.);
#7159=ORIENTED_EDGE('',*,*,#4956,.F.);
#7160=ORIENTED_EDGE('',*,*,#4957,.F.);
#7161=ORIENTED_EDGE('',*,*,#4958,.T.);
#7162=ORIENTED_EDGE('',*,*,#4955,.T.);
#7163=ORIENTED_EDGE('',*,*,#4958,.F.);
#7164=ORIENTED_EDGE('',*,*,#4957,.T.);
#7165=ORIENTED_EDGE('',*,*,#4934,.T.);
#7166=ORIENTED_EDGE('',*,*,#4938,.T.);
#7167=ORIENTED_EDGE('',*,*,#4947,.T.);
#7168=ORIENTED_EDGE('',*,*,#4945,.T.);
#7169=ORIENTED_EDGE('',*,*,#4926,.T.);
#7170=ORIENTED_EDGE('',*,*,#4932,.T.);
#7171=ORIENTED_EDGE('',*,*,#4942,.T.);
#7172=ORIENTED_EDGE('',*,*,#4959,.T.);
#7173=ORIENTED_EDGE('',*,*,#4960,.F.);
#7174=ORIENTED_EDGE('',*,*,#4961,.F.);
#7175=ORIENTED_EDGE('',*,*,#4959,.F.);
#7176=ORIENTED_EDGE('',*,*,#4944,.T.);
#7177=ORIENTED_EDGE('',*,*,#4940,.T.);
#7178=ORIENTED_EDGE('',*,*,#4900,.T.);
#7179=ORIENTED_EDGE('',*,*,#4906,.T.);
#7180=ORIENTED_EDGE('',*,*,#4908,.T.);
#7181=ORIENTED_EDGE('',*,*,#4912,.T.);
#7182=ORIENTED_EDGE('',*,*,#4914,.T.);
#7183=ORIENTED_EDGE('',*,*,#4918,.T.);
#7184=ORIENTED_EDGE('',*,*,#4920,.T.);
#7185=ORIENTED_EDGE('',*,*,#4924,.T.);
#7186=ORIENTED_EDGE('',*,*,#4952,.F.);
#7187=ORIENTED_EDGE('',*,*,#4962,.T.);
#7188=ORIENTED_EDGE('',*,*,#4960,.T.);
#7189=ORIENTED_EDGE('',*,*,#4961,.T.);
#7190=ORIENTED_EDGE('',*,*,#4962,.F.);
#7620=CYLINDRICAL_SURFACE('',#9057,0.496);
#7621=CYLINDRICAL_SURFACE('',#9068,0.496);
#7622=CYLINDRICAL_SURFACE('',#9078,0.496);
#7623=CYLINDRICAL_SURFACE('',#9084,0.496);
#7624=CYLINDRICAL_SURFACE('',#9105,0.839230484541328);
#7625=CYLINDRICAL_SURFACE('',#9109,0.96675);
#8040=ADVANCED_FACE('',(#878),#7620,.T.);
#8041=ADVANCED_FACE('',(#879),#431,.F.);
#8042=ADVANCED_FACE('',(#880),#432,.F.);
#8043=ADVANCED_FACE('',(#881),#433,.F.);
#8044=ADVANCED_FACE('',(#882),#7621,.T.);
#8045=ADVANCED_FACE('',(#883),#434,.F.);
#8046=ADVANCED_FACE('',(#884),#435,.F.);
#8047=ADVANCED_FACE('',(#885),#436,.F.);
#8048=ADVANCED_FACE('',(#886),#7622,.T.);
#8049=ADVANCED_FACE('',(#887),#437,.F.);
#8050=ADVANCED_FACE('',(#888),#7623,.T.);
#8051=ADVANCED_FACE('',(#889),#438,.F.);
#8052=ADVANCED_FACE('',(#890),#439,.F.);
#8053=ADVANCED_FACE('',(#891),#440,.F.);
#8054=ADVANCED_FACE('',(#892),#441,.F.);
#8055=ADVANCED_FACE('',(#893),#442,.F.);
#8056=ADVANCED_FACE('',(#894),#443,.F.);
#8057=ADVANCED_FACE('',(#895),#234,.F.);
#8058=ADVANCED_FACE('',(#896,#175),#444,.T.);
#8059=ADVANCED_FACE('',(#897),#7624,.T.);
#8060=ADVANCED_FACE('',(#898),#64,.T.);
#8061=ADVANCED_FACE('',(#899),#7625,.T.);
#8062=ADVANCED_FACE('',(#900),#445,.T.);
#8063=ADVANCED_FACE('',(#901),#211,.T.);
#8064=ADVANCED_FACE('',(#902),#65,.T.);
#8124=CLOSED_SHELL('',(#8040,#8041,#8042,#8043,#8044,#8045,#8046,#8047,
#8048,#8049,#8050,#8051,#8052,#8053,#8054,#8055,#8056,#8057,#8058,#8059,
#8060,#8061,#8062,#8063,#8064));
#9056=AXIS2_PLACEMENT_3D('',#16445,#11349,#11350);
#9057=AXIS2_PLACEMENT_3D('',#16446,#11351,#11352);
#9058=AXIS2_PLACEMENT_3D('',#16467,#11354,#11355);
#9059=AXIS2_PLACEMENT_3D('',#16469,#11356,#11357);
#9060=AXIS2_PLACEMENT_3D('',#16471,#11358,#11359);
#9061=AXIS2_PLACEMENT_3D('',#16473,#11361,#11362);
#9062=AXIS2_PLACEMENT_3D('',#16475,#11363,#11364);
#9063=AXIS2_PLACEMENT_3D('',#16477,#11366,#11367);
#9064=AXIS2_PLACEMENT_3D('',#16479,#11368,#11369);
#9065=AXIS2_PLACEMENT_3D('',#16483,#11371,#11372);
#9066=AXIS2_PLACEMENT_3D('',#16485,#11374,#11375);
#9067=AXIS2_PLACEMENT_3D('',#16487,#11376,#11377);
#9068=AXIS2_PLACEMENT_3D('',#16489,#11379,#11380);
#9069=AXIS2_PLACEMENT_3D('',#16507,#11381,#11382);
#9070=AXIS2_PLACEMENT_3D('',#16509,#11383,#11384);
#9071=AXIS2_PLACEMENT_3D('',#16511,#11386,#11387);
#9072=AXIS2_PLACEMENT_3D('',#16513,#11388,#11389);
#9073=AXIS2_PLACEMENT_3D('',#16515,#11391,#11392);
#9074=AXIS2_PLACEMENT_3D('',#16517,#11393,#11394);
#9075=AXIS2_PLACEMENT_3D('',#16521,#11396,#11397);
#9076=AXIS2_PLACEMENT_3D('',#16523,#11399,#11400);
#9077=AXIS2_PLACEMENT_3D('',#16525,#11401,#11402);
#9078=AXIS2_PLACEMENT_3D('',#16527,#11404,#11405);
#9079=AXIS2_PLACEMENT_3D('',#16548,#11407,#11408);
#9080=AXIS2_PLACEMENT_3D('',#16550,#11409,#11410);
#9081=AXIS2_PLACEMENT_3D('',#16552,#11411,#11412);
#9082=AXIS2_PLACEMENT_3D('',#16554,#11414,#11415);
#9083=AXIS2_PLACEMENT_3D('',#16556,#11416,#11417);
#9084=AXIS2_PLACEMENT_3D('',#16558,#11419,#11420);
#9085=AXIS2_PLACEMENT_3D('',#16576,#11421,#11422);
#9086=AXIS2_PLACEMENT_3D('',#16578,#11423,#11424);
#9087=AXIS2_PLACEMENT_3D('',#16580,#11426,#11427);
#9088=AXIS2_PLACEMENT_3D('',#16582,#11428,#11429);
#9089=AXIS2_PLACEMENT_3D('',#16584,#11431,#11432);
#9090=AXIS2_PLACEMENT_3D('',#16586,#11433,#11434);
#9091=AXIS2_PLACEMENT_3D('',#16588,#11436,#11437);
#9092=AXIS2_PLACEMENT_3D('',#16590,#11438,#11439);
#9093=AXIS2_PLACEMENT_3D('',#16592,#11441,#11442);
#9094=AXIS2_PLACEMENT_3D('',#16593,#11443,#11444);
#9095=AXIS2_PLACEMENT_3D('',#16595,#11445,#11446);
#9096=AXIS2_PLACEMENT_3D('',#16597,#11448,#11449);
#9097=AXIS2_PLACEMENT_3D('',#16598,#11450,#11451);
#9098=AXIS2_PLACEMENT_3D('',#16600,#11453,#11454);
#9099=AXIS2_PLACEMENT_3D('',#16601,#11455,#11456);
#9100=AXIS2_PLACEMENT_3D('',#16603,#11457,#11458);
#9101=AXIS2_PLACEMENT_3D('',#16605,#11459,#11460);
#9102=AXIS2_PLACEMENT_3D('',#16606,#11461,#11462);
#9103=AXIS2_PLACEMENT_3D('',#16607,#11463,#11464);
#9104=AXIS2_PLACEMENT_3D('',#16609,#11465,#11466);
#9105=AXIS2_PLACEMENT_3D('',#16610,#11467,#11468);
#9106=AXIS2_PLACEMENT_3D('',#16612,#11469,#11470);
#9107=AXIS2_PLACEMENT_3D('',#16614,#11472,#11473);
#9108=AXIS2_PLACEMENT_3D('',#16616,#11474,#11475);
#9109=AXIS2_PLACEMENT_3D('',#16618,#11477,#11478);
#9110=AXIS2_PLACEMENT_3D('',#16620,#11479,#11480);
#9111=AXIS2_PLACEMENT_3D('',#16622,#11482,#11483);
#9112=AXIS2_PLACEMENT_3D('',#16623,#11484,#11485);
#9113=AXIS2_PLACEMENT_3D('',#16625,#11486,#11487);
#9114=AXIS2_PLACEMENT_3D('',#16627,#11488,#11489);
#9115=AXIS2_PLACEMENT_3D('',#16628,#11490,#11491);
#9116=AXIS2_PLACEMENT_3D('',#16629,#11492,#11493);
#11349=DIRECTION('axis',(0.,0.,1.));
#11350=DIRECTION('refdir',(1.,0.,0.));
#11351=DIRECTION('center_axis',(0.,0.,-1.));
#11352=DIRECTION('ref_axis',(0.707106781186864,-0.707106781186231,0.));
#11353=DIRECTION('',(0.,0.,1.));
#11354=DIRECTION('center_axis',(-0.866025403784439,2.42308806056559E-16,
-0.5));
#11355=DIRECTION('ref_axis',(0.5,-1.39897054514259E-16,-0.866025403784439));
#11356=DIRECTION('center_axis',(0.,0.,-1.));
#11357=DIRECTION('ref_axis',(0.707106781186864,-0.707106781186231,0.));
#11358=DIRECTION('center_axis',(-1.34432925600244E-12,0.866025403784439,
-0.5));
#11359=DIRECTION('ref_axis',(7.76183832708735E-13,-0.5,-0.866025403784439));
#11360=DIRECTION('',(0.,0.,-1.));
#11361=DIRECTION('center_axis',(-1.,-8.96558844583498E-13,0.));
#11362=DIRECTION('ref_axis',(-8.96558844583498E-13,1.,0.));
#11363=DIRECTION('center_axis',(-1.,-8.96558844583498E-13,0.));
#11364=DIRECTION('ref_axis',(0.,0.,-1.));
#11365=DIRECTION('',(-4.48279422291749E-13,0.5,0.866025403784439));
#11366=DIRECTION('center_axis',(-1.34432925600244E-12,0.866025403784439,
-0.5));
#11367=DIRECTION('ref_axis',(1.,1.55229771566499E-12,0.));
#11368=DIRECTION('center_axis',(-1.34432925600244E-12,0.866025403784439,
-0.5));
#11369=DIRECTION('ref_axis',(0.,-0.5,-0.866025403784439));
#11370=DIRECTION('',(-1.,-1.55229771566499E-12,0.));
#11371=DIRECTION('center_axis',(-1.34432925600244E-12,0.866025403784439,
-0.5));
#11372=DIRECTION('ref_axis',(7.76183832708735E-13,-0.5,-0.866025403784439));
#11373=DIRECTION('',(7.28095205575773E-14,-0.5,-0.866025403784439));
#11374=DIRECTION('center_axis',(1.,1.45619041115155E-13,0.));
#11375=DIRECTION('ref_axis',(1.45619041115155E-13,-1.,0.));
#11376=DIRECTION('center_axis',(1.,1.45619041115155E-13,0.));
#11377=DIRECTION('ref_axis',(0.,0.,1.));
#11378=DIRECTION('',(0.,0.,1.));
#11379=DIRECTION('center_axis',(0.,0.,-1.));
#11380=DIRECTION('ref_axis',(-0.707106781186035,-0.70710678118706,0.));
#11381=DIRECTION('center_axis',(0.,0.,-1.));
#11382=DIRECTION('ref_axis',(-0.707106781186035,-0.70710678118706,0.));
#11383=DIRECTION('center_axis',(0.866025403784439,1.82700839766916E-13,
-0.5));
#11384=DIRECTION('ref_axis',(-0.5,-1.0551735336738E-13,-0.866025403784439));
#11385=DIRECTION('',(0.,0.,-1.));
#11386=DIRECTION('center_axis',(-1.30466679482154E-12,1.,0.));
#11387=DIRECTION('ref_axis',(1.,1.30466679482154E-12,0.));
#11388=DIRECTION('center_axis',(-1.30466679482154E-12,1.,0.));
#11389=DIRECTION('ref_axis',(0.,0.,-1.));
#11390=DIRECTION('',(0.5,6.52333397410772E-13,0.866025403784439));
#11391=DIRECTION('center_axis',(0.866025403784439,1.82700839766916E-13,
-0.5));
#11392=DIRECTION('ref_axis',(2.10964758041199E-13,-1.,0.));
#11393=DIRECTION('center_axis',(0.866025403784439,1.82700839766916E-13,
-0.5));
#11394=DIRECTION('ref_axis',(0.5,0.,0.866025403784439));
#11395=DIRECTION('',(-2.10964758041199E-13,1.,0.));
#11396=DIRECTION('center_axis',(0.866025403784439,1.82700839766916E-13,
-0.5));
#11397=DIRECTION('ref_axis',(-0.5,-1.05482379103751E-13,-0.866025403784439));
#11398=DIRECTION('',(-0.5,6.4832235838889E-13,-0.866025403784439));
#11399=DIRECTION('center_axis',(-1.29664471677778E-12,-1.,0.));
#11400=DIRECTION('ref_axis',(-1.,1.29664471677778E-12,0.));
#11401=DIRECTION('center_axis',(-1.29664471677778E-12,-1.,0.));
#11402=DIRECTION('ref_axis',(0.,0.,1.));
#11403=DIRECTION('',(0.,0.,1.));
#11404=DIRECTION('center_axis',(0.,0.,-1.));
#11405=DIRECTION('ref_axis',(0.707106781186895,0.7071067811862,0.));
#11406=DIRECTION('',(0.,0.,1.));
#11407=DIRECTION('center_axis',(-1.35644469630397E-12,-0.866025403784439,
-0.5));
#11408=DIRECTION('ref_axis',(7.8314371117082E-13,0.5,-0.866025403784439));
#11409=DIRECTION('center_axis',(0.,0.,-1.));
#11410=DIRECTION('ref_axis',(0.707106781186895,0.7071067811862,0.));
#11411=DIRECTION('center_axis',(-0.866025403784439,2.42308806056559E-16,
-0.5));
#11412=DIRECTION('ref_axis',(0.5,-1.39897054514259E-16,-0.866025403784439));
#11413=DIRECTION('',(0.,0.,-1.));
#11414=DIRECTION('center_axis',(1.80920256647203E-12,-1.,0.));
#11415=DIRECTION('ref_axis',(-1.,-1.80920256647203E-12,0.));
#11416=DIRECTION('center_axis',(1.80920256647203E-12,-1.,0.));
#11417=DIRECTION('ref_axis',(0.,0.,1.));
#11418=DIRECTION('',(-0.5,-9.04601283236015E-13,0.866025403784439));
#11419=DIRECTION('center_axis',(0.,0.,-1.));
#11420=DIRECTION('ref_axis',(-0.707106781186768,0.707106781186327,0.));
#11421=DIRECTION('center_axis',(0.,0.,-1.));
#11422=DIRECTION('ref_axis',(-0.707106781186768,0.707106781186327,0.));
#11423=DIRECTION('center_axis',(-1.35644469630397E-12,-0.866025403784439,
-0.5));
#11424=DIRECTION('ref_axis',(7.83108736907191E-13,0.5,-0.866025403784439));
#11425=DIRECTION('',(0.,0.,-1.));
#11426=DIRECTION('center_axis',(1.,1.91935343509834E-12,0.));
#11427=DIRECTION('ref_axis',(1.91935343509834E-12,-1.,0.));
#11428=DIRECTION('center_axis',(1.,1.91935343509834E-12,0.));
#11429=DIRECTION('ref_axis',(0.,0.,1.));
#11430=DIRECTION('',(9.59676717549172E-13,-0.5,0.866025403784439));
#11431=DIRECTION('center_axis',(-1.62884833462111E-16,1.,0.));
#11432=DIRECTION('ref_axis',(1.,1.62884833462111E-16,0.));
#11433=DIRECTION('center_axis',(-1.62884833462111E-16,1.,0.));
#11434=DIRECTION('ref_axis',(0.,0.,-1.));
#11435=DIRECTION('',(0.5,8.14424167310554E-17,-0.866025403784439));
#11436=DIRECTION('center_axis',(-0.866025403784439,2.42308806056559E-16,
-0.5));
#11437=DIRECTION('ref_axis',(2.79794108807543E-16,1.,0.));
#11438=DIRECTION('center_axis',(-0.866025403784439,2.42308806056559E-16,
-0.5));
#11439=DIRECTION('ref_axis',(0.5,0.,-0.866025403784439));
#11440=DIRECTION('',(-2.79794108807543E-16,-1.,0.));
#11441=DIRECTION('center_axis',(-0.866025403784439,2.42308806056559E-16,
-0.5));
#11442=DIRECTION('ref_axis',(0.5,0.,-0.866025403784439));
#11443=DIRECTION('center_axis',(-1.,2.79168316070879E-12,0.));
#11444=DIRECTION('ref_axis',(2.79168316070879E-12,1.,0.));
#11445=DIRECTION('center_axis',(-1.,2.79168316070879E-12,0.));
#11446=DIRECTION('ref_axis',(0.,0.,-1.));
#11447=DIRECTION('',(1.3958415803544E-12,0.5,-0.866025403784439));
#11448=DIRECTION('center_axis',(-1.35644469630397E-12,-0.866025403784439,
-0.5));
#11449=DIRECTION('ref_axis',(-1.,1.56628742110387E-12,0.));
#11450=DIRECTION('center_axis',(-1.35644469630397E-12,-0.866025403784439,
-0.5));
#11451=DIRECTION('ref_axis',(0.,-0.5,0.866025403784439));
#11452=DIRECTION('',(1.,-1.56628742110387E-12,0.));
#11453=DIRECTION('center_axis',(0.,0.,-1.));
#11454=DIRECTION('ref_axis',(-1.,0.,0.));
#11455=DIRECTION('center_axis',(0.,0.,-1.));
#11456=DIRECTION('ref_axis',(-1.,0.,0.));
#11457=DIRECTION('center_axis',(0.,0.,-1.));
#11458=DIRECTION('ref_axis',(1.,0.,0.));
#11459=DIRECTION('center_axis',(-1.22464679914735E-16,-1.,0.));
#11460=DIRECTION('ref_axis',(1.,-1.22464679914735E-16,0.));
#11461=DIRECTION('center_axis',(0.,0.,1.));
#11462=DIRECTION('ref_axis',(1.,0.,0.));
#11463=DIRECTION('center_axis',(0.,0.,-1.));
#11464=DIRECTION('ref_axis',(-1.,0.,0.));
#11465=DIRECTION('center_axis',(0.,0.,-1.));
#11466=DIRECTION('ref_axis',(1.,0.,0.));
#11467=DIRECTION('center_axis',(0.,0.,-1.));
#11468=DIRECTION('ref_axis',(-1.,0.,0.));
#11469=DIRECTION('center_axis',(0.,0.,-1.));
#11470=DIRECTION('ref_axis',(1.,0.,0.));
#11471=DIRECTION('',(0.,0.,1.));
#11472=DIRECTION('center_axis',(0.,0.,-1.));
#11473=DIRECTION('ref_axis',(-1.,0.,0.));
#11474=DIRECTION('center_axis',(0.,0.,-1.));
#11475=DIRECTION('ref_axis',(-1.,0.,0.));
#11476=DIRECTION('',(-0.258819045102519,3.16961915143174E-17,0.965925826289069));
#11477=DIRECTION('center_axis',(0.,0.,-1.));
#11478=DIRECTION('ref_axis',(-1.,0.,0.));
#11479=DIRECTION('center_axis',(0.,0.,1.));
#11480=DIRECTION('ref_axis',(-1.,0.,0.));
#11481=DIRECTION('',(0.,0.,1.));
#11482=DIRECTION('center_axis',(0.,0.,-1.));
#11483=DIRECTION('ref_axis',(-1.,0.,0.));
#11484=DIRECTION('center_axis',(6.12323399573676E-17,0.,1.));
#11485=DIRECTION('ref_axis',(1.,0.,0.));
#11486=DIRECTION('center_axis',(1.22464679914735E-16,-1.,0.));
#11487=DIRECTION('ref_axis',(-1.,-1.22464679914735E-16,0.));
#11488=DIRECTION('center_axis',(0.,0.,-1.));
#11489=DIRECTION('ref_axis',(1.,0.,0.));
#11490=DIRECTION('center_axis',(0.,0.,-1.));
#11491=DIRECTION('ref_axis',(1.,0.,0.));
#11492=DIRECTION('center_axis',(0.,0.,-1.));
#11493=DIRECTION('ref_axis',(-1.,0.,0.));
#11494=DIRECTION('',(-0.087155742757872,1.06735001395738E-17,0.996194698090852));
#16445=CARTESIAN_POINT('',(0.,0.,0.));
#16446=CARTESIAN_POINT('Origin',(-0.744000000195138,0.744000000196221,1.2));
#16447=CARTESIAN_POINT('',(-0.744000000195138,0.248000000196221,1.15122809938326));
#16448=CARTESIAN_POINT('',(-0.248000000195138,0.744000000196666,1.15122809938313));
#16449=CARTESIAN_POINT('Ctrl Pts',(-0.744000000195138,0.248000000196221,
1.15122809938326));
#16450=CARTESIAN_POINT('Ctrl Pts',(-0.743548129195526,0.248000000196221,
1.15128162561029));
#16451=CARTESIAN_POINT('Ctrl Pts',(-0.743096462399636,0.248000617700407,
1.15133505381795));
#16452=CARTESIAN_POINT('Ctrl Pts',(-0.68084251616827,0.248170686680912,
1.1586889909138));
#16453=CARTESIAN_POINT('Ctrl Pts',(-0.614748859330863,0.260619583354249,
1.16502989619583));
#16454=CARTESIAN_POINT('Ctrl Pts',(-0.492966510303847,0.311166686726808,
1.17344391775669));
#16455=CARTESIAN_POINT('Ctrl Pts',(-0.437280006866291,0.349270066587974,
1.17551763482271));
#16456=CARTESIAN_POINT('Ctrl Pts',(-0.393275036726453,0.393275036727851,
1.17551763482269));
#16457=CARTESIAN_POINT('Ctrl Pts',(-0.349270066586615,0.437280006867729,
1.17551763482268));
#16458=CARTESIAN_POINT('Ctrl Pts',(-0.3111666867255,0.49296651030532,1.17344391775664));
#16459=CARTESIAN_POINT('Ctrl Pts',(-0.26061958335305,0.61474885933238,1.16502989619573));
#16460=CARTESIAN_POINT('Ctrl Pts',(-0.248170686679772,0.680842516169798,
1.15868899091368));
#16461=CARTESIAN_POINT('Ctrl Pts',(-0.248000617699323,0.743096462401038,
1.15133505381783));
#16462=CARTESIAN_POINT('Ctrl Pts',(-0.248000000195138,0.743548129196929,
1.15128162561017));
#16463=CARTESIAN_POINT('Ctrl Pts',(-0.248000000195138,0.744000000196666,
1.15122809938313));
#16464=CARTESIAN_POINT('',(-0.744000000195138,0.248000000196221,0.583389912843141));
#16465=CARTESIAN_POINT('',(-0.744000000195138,0.248000000196221,1.2));
#16466=CARTESIAN_POINT('',(-0.516876228118667,0.303056928861888,0.19));
#16467=CARTESIAN_POINT('Origin',(-0.744000000195138,0.744000000196221,0.583389912843142));
#16468=CARTESIAN_POINT('',(-0.303056928861701,0.51687622811801,0.19));
#16469=CARTESIAN_POINT('Origin',(-0.744000000195138,0.744000000196221,0.19));
#16470=CARTESIAN_POINT('',(-0.248000000195138,0.744000000196666,0.583389912846777));
#16471=CARTESIAN_POINT('Origin',(-0.744000000195138,0.744000000196221,0.583389912847341));
#16472=CARTESIAN_POINT('',(-0.248000000195138,0.744000000196666,1.2));
#16473=CARTESIAN_POINT('Origin',(-0.248000000194694,0.24800000019315,1.2));
#16474=CARTESIAN_POINT('',(-0.24800000019541,1.04682989872245,1.10790668314437));
#16475=CARTESIAN_POINT('Origin',(-0.248000000194471,-2.22346593631069E-13,
-5.12965591734105));
#16476=CARTESIAN_POINT('',(-0.248000000195362,0.993500000023809,1.01553658903582));
#16477=CARTESIAN_POINT('Origin',(-0.248000000195457,1.09999999999962,1.2));
#16478=CARTESIAN_POINT('',(0.248000000196041,1.04682989872314,1.10790668314423));
#16479=CARTESIAN_POINT('Origin',(2.9811416492917E-12,-1.91582141081592,
-4.02355591008723));
#16480=CARTESIAN_POINT('',(0.303056928861511,0.516876228118951,0.19));
#16481=CARTESIAN_POINT('',(-0.124000000097707,0.516876228118288,0.19));
#16482=CARTESIAN_POINT('',(0.248000000196085,0.744000000194883,0.583389912842355));
#16483=CARTESIAN_POINT('Origin',(0.744000000196085,0.744000000194955,0.583389912841147));
#16484=CARTESIAN_POINT('',(0.248000000196033,1.1000000000003,1.19999999999985));
#16485=CARTESIAN_POINT('Origin',(0.248000000196033,1.10000000000039,1.2));
#16486=CARTESIAN_POINT('',(0.248000000196085,0.744000000194883,1.1512280993833));
#16487=CARTESIAN_POINT('Origin',(0.248000000196193,3.61135222251268E-14,
-5.12965591734105));
#16488=CARTESIAN_POINT('',(0.248000000196085,0.744000000194883,1.2));
#16489=CARTESIAN_POINT('Origin',(0.744000000196085,0.744000000194955,1.2));
#16490=CARTESIAN_POINT('',(0.744000000196732,0.248000000194955,1.15122809938313));
#16491=CARTESIAN_POINT('Ctrl Pts',(0.248000000196085,0.744000000194883,
1.1512280993833));
#16492=CARTESIAN_POINT('Ctrl Pts',(0.248000000196085,0.743548129195249,
1.15128162561033));
#16493=CARTESIAN_POINT('Ctrl Pts',(0.24800061770027,0.743096462399337,1.15133505381799));
#16494=CARTESIAN_POINT('Ctrl Pts',(0.248170686680793,0.68084251616795,1.15868899091384));
#16495=CARTESIAN_POINT('Ctrl Pts',(0.260619583354148,0.614748859330546,
1.16502989619587));
#16496=CARTESIAN_POINT('Ctrl Pts',(0.311166686726741,0.492966510303544,
1.17344391775672));
#16497=CARTESIAN_POINT('Ctrl Pts',(0.349270066587923,0.437280006865998,
1.17551763482273));
#16498=CARTESIAN_POINT('Ctrl Pts',(0.393275036727812,0.393275036726173,
1.17551763482271));
#16499=CARTESIAN_POINT('Ctrl Pts',(0.437280006867702,0.349270066586347,
1.1755176348227));
#16500=CARTESIAN_POINT('Ctrl Pts',(0.492966510305304,0.311166686725247,
1.17344391775665));
#16501=CARTESIAN_POINT('Ctrl Pts',(0.614748859332378,0.26061958335283,1.16502989619575));
#16502=CARTESIAN_POINT('Ctrl Pts',(0.6808425161698,0.248170686679572,1.15868899091369));
#16503=CARTESIAN_POINT('Ctrl Pts',(0.743096462401062,0.24800061769914,1.15133505381783));
#16504=CARTESIAN_POINT('Ctrl Pts',(0.743548129196974,0.248000000194955,
1.15128162561017));
#16505=CARTESIAN_POINT('Ctrl Pts',(0.744000000196732,0.248000000194955,
1.15122809938313));
#16506=CARTESIAN_POINT('',(0.516876228118432,0.30305692886123,0.19));
#16507=CARTESIAN_POINT('Origin',(0.744000000196085,0.744000000194955,0.19));
#16508=CARTESIAN_POINT('',(0.744000000196732,0.248000000194955,0.583389912846289));
#16509=CARTESIAN_POINT('Origin',(0.744000000196085,0.744000000194955,0.583389912845349));
#16510=CARTESIAN_POINT('',(0.744000000196732,0.248000000194955,1.2));
#16511=CARTESIAN_POINT('Origin',(0.248000000196157,0.248000000194308,1.2));
#16512=CARTESIAN_POINT('',(1.04682989872277,0.24800000019535,1.10790668314432));
#16513=CARTESIAN_POINT('Origin',(-3.16340915708764E-13,0.248000000193984,
-5.12965591734105));
#16514=CARTESIAN_POINT('',(0.99350000002449,0.248000000195281,1.01553658903639));
#16515=CARTESIAN_POINT('Origin',(1.09999999999997,0.248000000195419,1.2));
#16516=CARTESIAN_POINT('',(1.04682989872287,-0.248000000195507,1.1079066831443));
#16517=CARTESIAN_POINT('Origin',(-1.91582141081591,-4.04170800382928E-13,
-4.02355591008723));
#16518=CARTESIAN_POINT('',(0.51687622811856,-0.3030569288607,0.19));
#16519=CARTESIAN_POINT('',(0.51687622811847,0.124000000097702,0.19));
#16520=CARTESIAN_POINT('',(0.744000000195517,-0.248000000195115,0.583389912844004));
#16521=CARTESIAN_POINT('Origin',(0.744000000194874,-0.744000000195115,0.583389912842708));
#16522=CARTESIAN_POINT('',(1.09999999999998,-0.248000000195576,1.19999999999984));
#16523=CARTESIAN_POINT('Origin',(1.10000000000007,-0.248000000195576,1.2));
#16524=CARTESIAN_POINT('',(0.744000000195517,-0.248000000195115,1.15122809938326));
#16525=CARTESIAN_POINT('Origin',(-3.14351440352569E-13,-0.24800000019415,
-5.12965591734105));
#16526=CARTESIAN_POINT('',(0.744000000195517,-0.248000000195115,1.2));
#16527=CARTESIAN_POINT('Origin',(-0.744000000195415,-0.744000000194864,
1.2));
#16528=CARTESIAN_POINT('',(-0.248000000195415,-0.744000000196249,1.15122809938316));
#16529=CARTESIAN_POINT('',(-0.744000000196312,-0.248000000194864,1.15122809938318));
#16530=CARTESIAN_POINT('Ctrl Pts',(-0.248000000195415,-0.744000000196249,
1.15122809938316));
#16531=CARTESIAN_POINT('Ctrl Pts',(-0.248000000195414,-0.74354812919633,
1.15128162561023));
#16532=CARTESIAN_POINT('Ctrl Pts',(-0.248000617699598,-0.743096462400134,
1.15133505381792));
#16533=CARTESIAN_POINT('Ctrl Pts',(-0.248170686680046,-0.680842516168463,
1.15868899091381));
#16534=CARTESIAN_POINT('Ctrl Pts',(-0.260619583353321,-0.614748859331044,
1.16502989619585));
#16535=CARTESIAN_POINT('Ctrl Pts',(-0.311166686725766,-0.49296651030398,
1.17344391775673));
#16536=CARTESIAN_POINT('Ctrl Pts',(-0.349270066586879,-0.437280006866388,
1.17551763482276));
#16537=CARTESIAN_POINT('Ctrl Pts',(-0.393275036726715,-0.393275036726509,
1.17551763482276));
#16538=CARTESIAN_POINT('Ctrl Pts',(-0.437280006866551,-0.349270066586629,
1.17551763482276));
#16539=CARTESIAN_POINT('Ctrl Pts',(-0.492966510304106,-0.311166686725461,
1.17344391775673));
#16540=CARTESIAN_POINT('Ctrl Pts',(-0.61474885933112,-0.260619583352896,
1.16502989619586));
#16541=CARTESIAN_POINT('Ctrl Pts',(-0.680842516168527,-0.248170686679557,
1.15868899091382));
#16542=CARTESIAN_POINT('Ctrl Pts',(-0.743096462400073,-0.248000617699049,
1.15133505381795));
#16543=CARTESIAN_POINT('Ctrl Pts',(-0.74354812919627,-0.248000000194863,
1.15128162561025));
#16544=CARTESIAN_POINT('Ctrl Pts',(-0.744000000196312,-0.248000000194864,
1.15122809938318));
#16545=CARTESIAN_POINT('',(-0.248000000195415,-0.744000000196249,0.58338991284606));
#16546=CARTESIAN_POINT('',(-0.248000000195415,-0.744000000196249,1.2));
#16547=CARTESIAN_POINT('',(-0.303056928861281,-0.516876228118006,0.19));
#16548=CARTESIAN_POINT('Origin',(-0.744000000195415,-0.744000000194864,
0.583389912845007));
#16549=CARTESIAN_POINT('',(-0.516876228118667,-0.303056928860673,0.19));
#16550=CARTESIAN_POINT('Origin',(-0.744000000195415,-0.744000000194864,
0.19));
#16551=CARTESIAN_POINT('',(-0.744000000196312,-0.248000000194864,0.583389912845176));
#16552=CARTESIAN_POINT('Origin',(-0.744000000195415,-0.744000000194864,
0.583389912843621));
#16553=CARTESIAN_POINT('',(-0.744000000196312,-0.248000000194864,1.2));
#16554=CARTESIAN_POINT('Origin',(-0.24800000019403,-0.248000000193966,1.2));
#16555=CARTESIAN_POINT('',(-1.04682989872298,-0.248000000195412,1.10790668314428));
#16556=CARTESIAN_POINT('Origin',(4.5589868649524E-13,-0.248000000193518,
-5.12965591734105));
#16557=CARTESIAN_POINT('',(-0.993500000024419,-0.248000000195315,1.01553658903588));
#16558=CARTESIAN_POINT('Origin',(0.744000000194874,-0.744000000195115,1.2));
#16559=CARTESIAN_POINT('',(0.248000000194874,-0.744000000196067,1.15122809938321));
#16560=CARTESIAN_POINT('Ctrl Pts',(0.744000000195517,-0.248000000195115,
1.15122809938326));
#16561=CARTESIAN_POINT('Ctrl Pts',(0.743548129195714,-0.248000000195114,
1.15128162561031));
#16562=CARTESIAN_POINT('Ctrl Pts',(0.743096462399633,-0.248000617699299,
1.15133505381799));
#16563=CARTESIAN_POINT('Ctrl Pts',(0.680842516168076,-0.248170686679796,
1.15868899091386));
#16564=CARTESIAN_POINT('Ctrl Pts',(0.614748859330666,-0.260619583353124,
1.1650298961959));
#16565=CARTESIAN_POINT('Ctrl Pts',(0.492966510303643,-0.311166686725667,
1.17344391775676));
#16566=CARTESIAN_POINT('Ctrl Pts',(0.437280006866081,-0.349270066586825,
1.17551763482279));
#16567=CARTESIAN_POINT('Ctrl Pts',(0.393275036726237,-0.393275036726696,
1.17551763482278));
#16568=CARTESIAN_POINT('Ctrl Pts',(0.349270066586393,-0.437280006866568,
1.17551763482278));
#16569=CARTESIAN_POINT('Ctrl Pts',(0.31116668672527,-0.492966510304154,
1.17344391775674));
#16570=CARTESIAN_POINT('Ctrl Pts',(0.260619583352803,-0.614748859331208,
1.16502989619586));
#16571=CARTESIAN_POINT('Ctrl Pts',(0.248170686679517,-0.680842516168625,
1.15868899091381));
#16572=CARTESIAN_POINT('Ctrl Pts',(0.248000617699059,-0.743096462400057,
1.15133505381795));
#16573=CARTESIAN_POINT('Ctrl Pts',(0.248000000194873,-0.743548129196139,
1.15128162561027));
#16574=CARTESIAN_POINT('Ctrl Pts',(0.248000000194874,-0.744000000196067,
1.15122809938321));
#16575=CARTESIAN_POINT('',(0.30305692886038,-0.516876228118955,0.19));
#16576=CARTESIAN_POINT('Origin',(0.744000000194874,-0.744000000195115,0.19));
#16577=CARTESIAN_POINT('',(0.248000000194874,-0.744000000196067,0.5833899128444));
#16578=CARTESIAN_POINT('Origin',(0.744000000194874,-0.744000000195115,0.583389912841405));
#16579=CARTESIAN_POINT('',(0.248000000194874,-0.744000000196067,1.2));
#16580=CARTESIAN_POINT('Origin',(0.248000000193922,-0.248000000194471,1.2));
#16581=CARTESIAN_POINT('',(0.248000000195456,-1.04682989872316,1.10790668314425));
#16582=CARTESIAN_POINT('Origin',(0.248000000193446,4.75999652275667E-13,
-5.12965591734105));
#16583=CARTESIAN_POINT('',(0.248000000195353,-0.993500000024651,1.01553658903593));
#16584=CARTESIAN_POINT('Origin',(-1.10000000000019,0.248000000196221,1.2));
#16585=CARTESIAN_POINT('',(-1.04682989872296,0.248000000196221,1.10790668314426));
#16586=CARTESIAN_POINT('Origin',(7.17605422133295E-15,0.248000000196221,
-5.12965591734105));
#16587=CARTESIAN_POINT('',(-1.10000000000019,0.248000000196221,1.2));
#16588=CARTESIAN_POINT('Origin',(-1.10000000000019,-0.248000000195508,1.2));
#16589=CARTESIAN_POINT('',(-1.04942373620595,-1.28517341949389E-16,1.11239934145138));
#16590=CARTESIAN_POINT('Origin',(1.91582141081578,-5.36035544273609E-16,
-4.02355591008731));
#16591=CARTESIAN_POINT('',(-0.516876228118667,-0.124000000097755,0.19));
#16592=CARTESIAN_POINT('Origin',(1.91582141081578,-5.36035544273609E-16,
-4.02355591008731));
#16593=CARTESIAN_POINT('Origin',(-0.248000000196409,-1.09999999999961,1.2));
#16594=CARTESIAN_POINT('',(-0.24800000019626,-1.04682989872243,1.10790668314434));
#16595=CARTESIAN_POINT('Origin',(-0.248000000193338,6.92337424395539E-13,
-5.12965591734105));
#16596=CARTESIAN_POINT('',(-0.248000000196409,-1.09999999999954,1.19999999999987));
#16597=CARTESIAN_POINT('Origin',(0.248000000195558,-1.10000000000039,1.2));
#16598=CARTESIAN_POINT('Origin',(3.00794342650252E-12,1.91582141081592,
-4.02355591008723));
#16599=CARTESIAN_POINT('',(0.124000000097801,-0.516876228118675,0.19));
#16600=CARTESIAN_POINT('Origin',(-5.91193760612896E-14,-1.66533453693773E-15,
0.19));
#16601=CARTESIAN_POINT('Origin',(0.,0.,-0.1));
#16602=CARTESIAN_POINT('',(0.939230484541328,-1.15022560655515E-16,0.));
#16603=CARTESIAN_POINT('Origin',(0.,0.,0.));
#16604=CARTESIAN_POINT('',(0.839230484541328,-1.02776092664042E-16,-0.1));
#16605=CARTESIAN_POINT('Origin',(0.939230484541328,-1.15022560655515E-16,
-0.1));
#16606=CARTESIAN_POINT('Origin',(0.,0.,-0.1));
#16607=CARTESIAN_POINT('Origin',(-0.839230484541328,0.,-7.24797437703358E-18));
#16608=CARTESIAN_POINT('',(2.15,-2.63299061816681E-16,0.));
#16609=CARTESIAN_POINT('Origin',(0.,0.,0.));
#16610=CARTESIAN_POINT('Origin',(0.,0.,-0.0749999999999998));
#16611=CARTESIAN_POINT('',(0.839230484541328,-1.02776092664042E-16,-0.15));
#16612=CARTESIAN_POINT('Origin',(0.,0.,-0.15));
#16613=CARTESIAN_POINT('',(0.839230484541328,-1.02776092664042E-16,-0.0749999999999998));
#16614=CARTESIAN_POINT('Origin',(0.,0.,-0.45));
#16615=CARTESIAN_POINT('',(0.96675,-1.1839272930757E-16,-0.625909310648334));
#16616=CARTESIAN_POINT('Origin',(0.,0.,-0.625909310648334));
#16617=CARTESIAN_POINT('',(0.919615242270664,-1.12620386289389E-16,-0.45));
#16618=CARTESIAN_POINT('Origin',(0.,0.,-3.375));
#16619=CARTESIAN_POINT('',(0.96675,1.1839272930757E-16,-6.));
#16620=CARTESIAN_POINT('Origin',(0.,0.,-6.));
#16621=CARTESIAN_POINT('',(0.96675,-1.1839272930757E-16,-3.375));
#16622=CARTESIAN_POINT('Origin',(0.,0.,-6.));
#16623=CARTESIAN_POINT('Origin',(7.21644966006352E-15,0.,-5.12965591734105));
#16624=CARTESIAN_POINT('',(-2.07563463599418,0.,0.85));
#16625=CARTESIAN_POINT('Origin',(7.21644966006352E-15,0.,-5.12965591734105));
#16626=CARTESIAN_POINT('',(2.07563463599418,-2.54191931316966E-16,0.85));
#16627=CARTESIAN_POINT('Origin',(0.,0.,0.85));
#16628=CARTESIAN_POINT('Origin',(0.,0.,0.85));
#16629=CARTESIAN_POINT('Origin',(0.,0.,0.425));
#16630=CARTESIAN_POINT('',(2.11281731799709,-2.58745496566823E-16,0.425));
#17025=UNCERTAINTY_MEASURE_WITH_UNIT(LENGTH_MEASURE(0.01),#17043,
'DISTANCE_ACCURACY_VALUE',
'Maximum model space distance between geometric entities at asserted c
onnectivities');
#17028=UNCERTAINTY_MEASURE_WITH_UNIT(LENGTH_MEASURE(0.01),#17043,
'DISTANCE_ACCURACY_VALUE',
'Maximum model space distance between geometric entities at asserted c
onnectivities');
#17039=(
GEOMETRIC_REPRESENTATION_CONTEXT(3)
GLOBAL_UNCERTAINTY_ASSIGNED_CONTEXT((#17025))
GLOBAL_UNIT_ASSIGNED_CONTEXT((#17043,#17045,#17046))
REPRESENTATION_CONTEXT('','3D')
);
#17042=(
GEOMETRIC_REPRESENTATION_CONTEXT(3)
GLOBAL_UNCERTAINTY_ASSIGNED_CONTEXT((#17028))
GLOBAL_UNIT_ASSIGNED_CONTEXT((#17043,#17045,#17046))
REPRESENTATION_CONTEXT('','3D')
);
#17043=(
LENGTH_UNIT()
NAMED_UNIT(*)
SI_UNIT(.MILLI.,.METRE.)
);
#17045=(
NAMED_UNIT(*)
PLANE_ANGLE_UNIT()
SI_UNIT($,.RADIAN.)
);
#17046=(
NAMED_UNIT(*)
SI_UNIT($,.STERADIAN.)
SOLID_ANGLE_UNIT()
);
#17057=SHAPE_DEFINITION_REPRESENTATION(#17070,#17095);
#17070=PRODUCT_DEFINITION_SHAPE('',$,#17109);
#17095=SHAPE_REPRESENTATION('',(#9056),#17039);
#17098=PRODUCT_DEFINITION_CONTEXT('part definition',#17139,'design');
#17109=PRODUCT_DEFINITION('BHS JIS B 1111 - M2x6 Steel 4.6 Plain_1',
'Binding Head Screw JIS B 1111 - M2x6 Steel 4.6 Plain v1 (2)',#17122,#17098);
#17122=PRODUCT_DEFINITION_FORMATION('',$,#17151);
#17139=APPLICATION_CONTEXT(
'Core Data for Automotive Mechanical Design Process');
#17140=PRODUCT_CONTEXT('part definition',#17139,'mechanical');
#17151=PRODUCT('BHS JIS B 1111 - M2x6 Steel 4.6 Plain_1',
'Binding Head Screw JIS B 1111 - M2x6 Steel 4.6 Plain v1 (2)',
'Binding Head Screw JIS B 1111 - M2x6',(#17140));
#17154=PRESENTATION_STYLE_ASSIGNMENT((#17155));
#17155=SURFACE_STYLE_USAGE(.BOTH.,#17156);
#17156=SURFACE_SIDE_STYLE('',(#17157));
#17157=SURFACE_STYLE_FILL_AREA(#17158);
#17158=FILL_AREA_STYLE('Steel - Satin',(#17159));
#17159=FILL_AREA_STYLE_COLOUR('Steel - Satin',#17160);
#17160=COLOUR_RGB('Steel - Satin', 0.09019608, 0.27058824, 0.51372549);
ENDSEC;
END-ISO-10303-21;
